ISO-10303-21;
HEADER;
/* Generated by software containing ST-Developer
 * from STEP Tools, Inc. (www.steptools.com) 
 */

FILE_DESCRIPTION(
/* description */ ('Torque wrench calibration arm'),
/* implementation_level */ '2;1');

FILE_NAME(
/* name */ 'Hanger keeper (1).step',
/* time_stamp */ '2026-10-28T03:24:52-07:00',
/* author */ (''),
/* organization */ (''),
/* preprocessor_version */ 'ST-DEVELOPER v20.2',
/* originating_system */ 'Autodesk Translation Framework v15.17.0.0',
/* authorisation */ '');

FILE_SCHEMA (('AUTOMOTIVE_DESIGN { 1 0 10303 214 3 1 1 }'));
ENDSEC;

DATA;
#10=MECHANICAL_DESIGN_GEOMETRIC_PRESENTATION_REPRESENTATION('',(#478),#12783);
#387=SHAPE_REPRESENTATION_RELATIONSHIP('SRR','None',#12972,#424);
#424=ADVANCED_BREP_SHAPE_REPRESENTATION('',(#530),#12781);
#478=STYLED_ITEM('',(#13205),#530);
#530=MANIFOLD_SOLID_BREP('Body1',#6549);
#649=FACE_BOUND('',#1766,.T.);
#650=FACE_BOUND('',#1768,.T.);
#862=PLANE('',#7771);
#863=PLANE('',#7772);
#1250=FACE_OUTER_BOUND('',#1763,.T.);
#1251=FACE_OUTER_BOUND('',#1764,.T.);
#1252=FACE_OUTER_BOUND('',#1765,.T.);
#1253=FACE_OUTER_BOUND('',#1767,.T.);
#1763=EDGE_LOOP('',(#5915,#5916,#5917,#5918));
#1764=EDGE_LOOP('',(#5919,#5920,#5921,#5922));
#1765=EDGE_LOOP('',(#5923));
#1766=EDGE_LOOP('',(#5924));
#1767=EDGE_LOOP('',(#5925));
#1768=EDGE_LOOP('',(#5926));
#2176=LINE('',#12607,#2591);
#2177=LINE('',#12613,#2592);
#2591=VECTOR('',#9814,0.225000000000001);
#2592=VECTOR('',#9821,0.799999999999997);
#2960=CIRCLE('',#7766,0.225000000000001);
#2961=CIRCLE('',#7767,0.225000000000001);
#2962=CIRCLE('',#7769,0.799999999999997);
#2963=CIRCLE('',#7770,0.799999999999997);
#3510=VERTEX_POINT('',#12604);
#3511=VERTEX_POINT('',#12606);
#3512=VERTEX_POINT('',#12610);
#3513=VERTEX_POINT('',#12612);
#4315=EDGE_CURVE('',#3510,#3510,#2960,.T.);
#4316=EDGE_CURVE('',#3510,#3511,#2176,.T.);
#4317=EDGE_CURVE('',#3511,#3511,#2961,.T.);
#4318=EDGE_CURVE('',#3512,#3512,#2962,.T.);
#4319=EDGE_CURVE('',#3512,#3513,#2177,.T.);
#4320=EDGE_CURVE('',#3513,#3513,#2963,.T.);
#5915=ORIENTED_EDGE('',*,*,#4315,.F.);
#5916=ORIENTED_EDGE('',*,*,#4316,.T.);
#5917=ORIENTED_EDGE('',*,*,#4317,.T.);
#5918=ORIENTED_EDGE('',*,*,#4316,.F.);
#5919=ORIENTED_EDGE('',*,*,#4318,.F.);
#5920=ORIENTED_EDGE('',*,*,#4319,.T.);
#5921=ORIENTED_EDGE('',*,*,#4320,.T.);
#5922=ORIENTED_EDGE('',*,*,#4319,.F.);
#5923=ORIENTED_EDGE('',*,*,#4318,.T.);
#5924=ORIENTED_EDGE('',*,*,#4315,.T.);
#5925=ORIENTED_EDGE('',*,*,#4320,.F.);
#5926=ORIENTED_EDGE('',*,*,#4317,.F.);
#6096=CYLINDRICAL_SURFACE('',#7765,0.225000000000001);
#6097=CYLINDRICAL_SURFACE('',#7768,0.799999999999997);
#6475=ADVANCED_FACE('',(#1250),#6096,.F.);
#6476=ADVANCED_FACE('',(#1251),#6097,.T.);
#6477=ADVANCED_FACE('',(#1252,#649),#862,.T.);
#6478=ADVANCED_FACE('',(#1253,#650),#863,.F.);
#6549=CLOSED_SHELL('',(#6475,#6476,#6477,#6478));
#7764=AXIS2_PLACEMENT_3D('',#12602,#9808,#9809);
#7765=AXIS2_PLACEMENT_3D('',#12603,#9810,#9811);
#7766=AXIS2_PLACEMENT_3D('',#12605,#9812,#9813);
#7767=AXIS2_PLACEMENT_3D('',#12608,#9815,#9816);
#7768=AXIS2_PLACEMENT_3D('',#12609,#9817,#9818);
#7769=AXIS2_PLACEMENT_3D('',#12611,#9819,#9820);
#7770=AXIS2_PLACEMENT_3D('',#12614,#9822,#9823);
#7771=AXIS2_PLACEMENT_3D('',#12615,#9824,#9825);
#7772=AXIS2_PLACEMENT_3D('',#12616,#9826,#9827);
#9808=DIRECTION('axis',(0.,0.,1.));
#9809=DIRECTION('refdir',(1.,0.,0.));
#9810=DIRECTION('center_axis',(0.,1.,0.));
#9811=DIRECTION('ref_axis',(1.,0.,0.));
#9812=DIRECTION('center_axis',(0.,-1.,0.));
#9813=DIRECTION('ref_axis',(1.,0.,0.));
#9814=DIRECTION('',(0.,-1.,0.));
#9815=DIRECTION('center_axis',(0.,-1.,0.));
#9816=DIRECTION('ref_axis',(1.,0.,0.));
#9817=DIRECTION('center_axis',(0.,1.,0.));
#9818=DIRECTION('ref_axis',(1.,0.,0.));
#9819=DIRECTION('center_axis',(0.,1.,0.));
#9820=DIRECTION('ref_axis',(1.,0.,0.));
#9821=DIRECTION('',(0.,-1.,0.));
#9822=DIRECTION('center_axis',(0.,1.,0.));
#9823=DIRECTION('ref_axis',(1.,0.,0.));
#9824=DIRECTION('center_axis',(0.,1.,0.));
#9825=DIRECTION('ref_axis',(1.,0.,0.));
#9826=DIRECTION('center_axis',(0.,1.,0.));
#9827=DIRECTION('ref_axis',(1.,0.,0.));
#12602=CARTESIAN_POINT('',(0.,0.,0.));
#12603=CARTESIAN_POINT('Origin',(50.,10.4,8.));
#12604=CARTESIAN_POINT('',(49.775,10.6,8.));
#12605=CARTESIAN_POINT('Origin',(50.,10.6,8.));
#12606=CARTESIAN_POINT('',(49.775,10.4,8.));
#12607=CARTESIAN_POINT('',(49.775,10.4,8.));
#12608=CARTESIAN_POINT('Origin',(50.,10.4,8.));
#12609=CARTESIAN_POINT('Origin',(50.,10.4,8.));
#12610=CARTESIAN_POINT('',(49.2,10.6,8.));
#12611=CARTESIAN_POINT('Origin',(50.,10.6,8.));
#12612=CARTESIAN_POINT('',(49.2,10.4,8.));
#12613=CARTESIAN_POINT('',(49.2,10.4,8.));
#12614=CARTESIAN_POINT('Origin',(50.,10.4,8.));
#12615=CARTESIAN_POINT('Origin',(50.,10.6,8.));
#12616=CARTESIAN_POINT('Origin',(50.,10.4,8.));
#12737=UNCERTAINTY_MEASURE_WITH_UNIT(LENGTH_MEASURE(0.001),#12784,
'DISTANCE_ACCURACY_VALUE',
'Maximum model space distance between geometric entities at asserted c
onnectivities');
#12739=UNCERTAINTY_MEASURE_WITH_UNIT(LENGTH_MEASURE(0.001),#12784,
'DISTANCE_ACCURACY_VALUE',
'Maximum model space distance between geometric entities at asserted c
onnectivities');
#12781=(
GEOMETRIC_REPRESENTATION_CONTEXT(3)
GLOBAL_UNCERTAINTY_ASSIGNED_CONTEXT((#12737))
GLOBAL_UNIT_ASSIGNED_CONTEXT((#12784,#12786,#12787))
REPRESENTATION_CONTEXT('','3D')
);
#12783=(
GEOMETRIC_REPRESENTATION_CONTEXT(3)
GLOBAL_UNCERTAINTY_ASSIGNED_CONTEXT((#12739))
GLOBAL_UNIT_ASSIGNED_CONTEXT((#12784,#12786,#12787))
REPRESENTATION_CONTEXT('','3D')
);
#12784=(
LENGTH_UNIT()
NAMED_UNIT(*)
SI_UNIT(.CENTI.,.METRE.)
);
#12786=(
NAMED_UNIT(*)
PLANE_ANGLE_UNIT()
SI_UNIT($,.RADIAN.)
);
#12787=(
NAMED_UNIT(*)
SI_UNIT($,.STERADIAN.)
SOLID_ANGLE_UNIT()
);
#12829=SHAPE_DEFINITION_REPRESENTATION(#12916,#12972);
#12916=PRODUCT_DEFINITION_SHAPE('',$,#13016);
#12972=SHAPE_REPRESENTATION('',(#7764),#12781);
#12974=PRODUCT_DEFINITION_CONTEXT('part definition',#13105,'design');
#13016=PRODUCT_DEFINITION('Hanger keeper (1)','Hanger keeper (1)',#13059,
#12974);
#13059=PRODUCT_DEFINITION_FORMATION('',$,#13148);
#13105=APPLICATION_CONTEXT(
'Core Data for Automotive Mechanical Design Process');
#13106=PRODUCT_CONTEXT('part definition',#13105,'mechanical');
#13148=PRODUCT('Hanger keeper (1)','Hanger keeper (1)','Hanger keeper (1)',(#13106));
#13199=COLOUR_RGB('Sky Blue',0.24,0.69,0.87);
#13200=FILL_AREA_STYLE_COLOUR('',#13199);
#13201=FILL_AREA_STYLE('',(#13200));
#13202=SURFACE_STYLE_FILL_AREA(#13201);
#13203=SURFACE_SIDE_STYLE('',(#13202));
#13204=SURFACE_STYLE_USAGE(.BOTH.,#13203);
#13205=PRESENTATION_STYLE_ASSIGNMENT((#13204));
ENDSEC;
END-ISO-10303-21;
